ISO-10303-21;
HEADER;
/* Generated by software containing ST-Developer
 * from STEP Tools, Inc. (www.steptools.com) 
 */

FILE_DESCRIPTION(
/* description */ ('Hand-crank gear train demonstrator'),
/* implementation_level */ '2;1');

FILE_NAME(
/* name */ 'Cap Screw - M4x16.step',
/* time_stamp */ '2026-10-28T03:22:13-07:00',
/* author */ (''),
/* organization */ (''),
/* preprocessor_version */ 'ST-DEVELOPER v20.2',
/* originating_system */ 'Autodesk Translation Framework v15.17.0.0',
/* authorisation */ '');

FILE_SCHEMA (('AUTOMOTIVE_DESIGN { 1 0 10303 214 3 1 1 }'));
ENDSEC;

DATA;
#10=MECHANICAL_DESIGN_GEOMETRIC_PRESENTATION_REPRESENTATION('',(#1266),#62758);
#1047=CONICAL_SURFACE('',#18686,0.325,0.785398163397448);
#1048=CONICAL_SURFACE('',#18690,0.335,0.785398163397448);
#1049=CONICAL_SURFACE('',#18694,0.21,0.463647609000806);
#1050=CONICAL_SURFACE('',#18698,0.18,0.785398163397448);
#1055=ORIENTED_CLOSED_SHELL('',*,#16451,.F.);
#1060=BREP_WITH_VOIDS('Body1',#16450,(#1055));
#1123=SHAPE_REPRESENTATION_RELATIONSHIP('SRR','None',#63101,#1187);
#1187=ADVANCED_BREP_SHAPE_REPRESENTATION('',(#1060),#62755);
#1266=STYLED_ITEM('',(#63469),#1060);
#1630=FACE_BOUND('',#4267,.T.);
#2110=PLANE('',#18684);
#2111=PLANE('',#18692);
#2112=PLANE('',#18700);
#2113=PLANE('',#18701);
#2114=PLANE('',#18702);
#2115=PLANE('',#18703);
#2116=PLANE('',#18704);
#2117=PLANE('',#18705);
#2118=PLANE('',#18706);
#2119=PLANE('',#18707);
#2120=PLANE('',#18708);
#3038=FACE_OUTER_BOUND('',#4262,.T.);
#3039=FACE_OUTER_BOUND('',#4263,.T.);
#3040=FACE_OUTER_BOUND('',#4264,.T.);
#3041=FACE_OUTER_BOUND('',#4265,.T.);
#3042=FACE_OUTER_BOUND('',#4266,.T.);
#3043=FACE_OUTER_BOUND('',#4268,.T.);
#3044=FACE_OUTER_BOUND('',#4269,.T.);
#3045=FACE_OUTER_BOUND('',#4270,.T.);
#3046=FACE_OUTER_BOUND('',#4271,.T.);
#3047=FACE_OUTER_BOUND('',#4272,.T.);
#3048=FACE_OUTER_BOUND('',#4273,.T.);
#3049=FACE_OUTER_BOUND('',#4274,.T.);
#3050=FACE_OUTER_BOUND('',#4275,.T.);
#3051=FACE_OUTER_BOUND('',#4276,.T.);
#3052=FACE_OUTER_BOUND('',#4277,.T.);
#3053=FACE_OUTER_BOUND('',#4278,.T.);
#3054=FACE_OUTER_BOUND('',#4279,.T.);
#4262=EDGE_LOOP('',(#15091));
#4263=EDGE_LOOP('',(#15092,#15093,#15094,#15095));
#4264=EDGE_LOOP('',(#15096,#15097,#15098,#15099));
#4265=EDGE_LOOP('',(#15100,#15101,#15102,#15103));
#4266=EDGE_LOOP('',(#15104));
#4267=EDGE_LOOP('',(#15105));
#4268=EDGE_LOOP('',(#15106,#15107,#15108,#15109));
#4269=EDGE_LOOP('',(#15110,#15111,#15112,#15113));
#4270=EDGE_LOOP('',(#15114,#15115,#15116,#15117));
#4271=EDGE_LOOP('',(#15118));
#4272=EDGE_LOOP('',(#15119,#15120,#15121,#15122));
#4273=EDGE_LOOP('',(#15123,#15124,#15125,#15126));
#4274=EDGE_LOOP('',(#15127,#15128,#15129,#15130));
#4275=EDGE_LOOP('',(#15131,#15132,#15133,#15134));
#4276=EDGE_LOOP('',(#15135,#15136,#15137,#15138));
#4277=EDGE_LOOP('',(#15139,#15140,#15141,#15142));
#4278=EDGE_LOOP('',(#15143,#15144,#15145,#15146,#15147,#15148));
#4279=EDGE_LOOP('',(#15149,#15150,#15151,#15152,#15153,#15154));
#5392=LINE('',#62420,#6524);
#5393=LINE('',#62424,#6525);
#5394=LINE('',#62428,#6526);
#5395=LINE('',#62435,#6527);
#5396=LINE('',#62439,#6528);
#5397=LINE('',#62443,#6529);
#5398=LINE('',#62448,#6530);
#5399=LINE('',#62450,#6531);
#5400=LINE('',#62452,#6532);
#5401=LINE('',#62453,#6533);
#5402=LINE('',#62456,#6534);
#5403=LINE('',#62458,#6535);
#5404=LINE('',#62459,#6536);
#5405=LINE('',#62462,#6537);
#5406=LINE('',#62464,#6538);
#5407=LINE('',#62465,#6539);
#5408=LINE('',#62468,#6540);
#5409=LINE('',#62470,#6541);
#5410=LINE('',#62471,#6542);
#5411=LINE('',#62474,#6543);
#5412=LINE('',#62476,#6544);
#5413=LINE('',#62477,#6545);
#5414=LINE('',#62479,#6546);
#5415=LINE('',#62480,#6547);
#6524=VECTOR('',#22997,0.325);
#6525=VECTOR('',#23002,0.35);
#6526=VECTOR('',#23007,0.335);
#6527=VECTOR('',#23016,0.21);
#6528=VECTOR('',#23021,0.2);
#6529=VECTOR('',#23026,0.18);
#6530=VECTOR('',#23031,1.);
#6531=VECTOR('',#23032,1.);
#6532=VECTOR('',#23033,1.);
#6533=VECTOR('',#23034,1.);
#6534=VECTOR('',#23037,1.);
#6535=VECTOR('',#23038,1.);
#6536=VECTOR('',#23039,1.);
#6537=VECTOR('',#23042,1.);
#6538=VECTOR('',#23043,1.);
#6539=VECTOR('',#23044,1.);
#6540=VECTOR('',#23047,1.);
#6541=VECTOR('',#23048,1.);
#6542=VECTOR('',#23049,1.);
#6543=VECTOR('',#23052,1.);
#6544=VECTOR('',#23053,1.);
#6545=VECTOR('',#23054,1.);
#6546=VECTOR('',#23057,1.);
#6547=VECTOR('',#23058,1.);
#7200=CIRCLE('',#18685,0.3);
#7201=CIRCLE('',#18687,0.35);
#7202=CIRCLE('',#18689,0.35);
#7203=CIRCLE('',#18691,0.32);
#7204=CIRCLE('',#18693,0.22);
#7205=CIRCLE('',#18695,0.1954);
#7206=CIRCLE('',#18697,0.1954);
#7207=CIRCLE('',#18699,0.16);
#8645=VERTEX_POINT('',#62415);
#8646=VERTEX_POINT('',#62418);
#8647=VERTEX_POINT('',#62422);
#8648=VERTEX_POINT('',#62426);
#8649=VERTEX_POINT('',#62430);
#8650=VERTEX_POINT('',#62433);
#8651=VERTEX_POINT('',#62437);
#8652=VERTEX_POINT('',#62441);
#8653=VERTEX_POINT('',#62446);
#8654=VERTEX_POINT('',#62447);
#8655=VERTEX_POINT('',#62449);
#8656=VERTEX_POINT('',#62451);
#8657=VERTEX_POINT('',#62455);
#8658=VERTEX_POINT('',#62457);
#8659=VERTEX_POINT('',#62461);
#8660=VERTEX_POINT('',#62463);
#8661=VERTEX_POINT('',#62467);
#8662=VERTEX_POINT('',#62469);
#8663=VERTEX_POINT('',#62473);
#8664=VERTEX_POINT('',#62475);
#10797=EDGE_CURVE('',#8645,#8645,#7200,.T.);
#10798=EDGE_CURVE('',#8646,#8646,#7201,.T.);
#10799=EDGE_CURVE('',#8646,#8645,#5392,.T.);
#10800=EDGE_CURVE('',#8647,#8647,#7202,.T.);
#10801=EDGE_CURVE('',#8647,#8646,#5393,.T.);
#10802=EDGE_CURVE('',#8648,#8648,#7203,.T.);
#10803=EDGE_CURVE('',#8648,#8647,#5394,.T.);
#10804=EDGE_CURVE('',#8649,#8649,#7204,.T.);
#10805=EDGE_CURVE('',#8650,#8650,#7205,.F.);
#10806=EDGE_CURVE('',#8650,#8649,#5395,.T.);
#10807=EDGE_CURVE('',#8651,#8651,#7206,.F.);
#10808=EDGE_CURVE('',#8651,#8650,#5396,.T.);
#10809=EDGE_CURVE('',#8652,#8652,#7207,.T.);
#10810=EDGE_CURVE('',#8652,#8651,#5397,.T.);
#10811=EDGE_CURVE('',#8653,#8654,#5398,.T.);
#10812=EDGE_CURVE('',#8654,#8655,#5399,.T.);
#10813=EDGE_CURVE('',#8655,#8656,#5400,.T.);
#10814=EDGE_CURVE('',#8653,#8656,#5401,.T.);
#10815=EDGE_CURVE('',#8654,#8657,#5402,.T.);
#10816=EDGE_CURVE('',#8657,#8658,#5403,.T.);
#10817=EDGE_CURVE('',#8658,#8655,#5404,.T.);
#10818=EDGE_CURVE('',#8657,#8659,#5405,.T.);
#10819=EDGE_CURVE('',#8659,#8660,#5406,.T.);
#10820=EDGE_CURVE('',#8660,#8658,#5407,.T.);
#10821=EDGE_CURVE('',#8659,#8661,#5408,.T.);
#10822=EDGE_CURVE('',#8661,#8662,#5409,.T.);
#10823=EDGE_CURVE('',#8662,#8660,#5410,.T.);
#10824=EDGE_CURVE('',#8661,#8663,#5411,.T.);
#10825=EDGE_CURVE('',#8663,#8664,#5412,.T.);
#10826=EDGE_CURVE('',#8664,#8662,#5413,.T.);
#10827=EDGE_CURVE('',#8663,#8653,#5414,.T.);
#10828=EDGE_CURVE('',#8656,#8664,#5415,.T.);
#15091=ORIENTED_EDGE('',*,*,#10797,.F.);
#15092=ORIENTED_EDGE('',*,*,#10798,.F.);
#15093=ORIENTED_EDGE('',*,*,#10799,.T.);
#15094=ORIENTED_EDGE('',*,*,#10797,.T.);
#15095=ORIENTED_EDGE('',*,*,#10799,.F.);
#15096=ORIENTED_EDGE('',*,*,#10800,.F.);
#15097=ORIENTED_EDGE('',*,*,#10801,.T.);
#15098=ORIENTED_EDGE('',*,*,#10798,.T.);
#15099=ORIENTED_EDGE('',*,*,#10801,.F.);
#15100=ORIENTED_EDGE('',*,*,#10802,.F.);
#15101=ORIENTED_EDGE('',*,*,#10803,.T.);
#15102=ORIENTED_EDGE('',*,*,#10800,.T.);
#15103=ORIENTED_EDGE('',*,*,#10803,.F.);
#15104=ORIENTED_EDGE('',*,*,#10802,.T.);
#15105=ORIENTED_EDGE('',*,*,#10804,.F.);
#15106=ORIENTED_EDGE('',*,*,#10805,.F.);
#15107=ORIENTED_EDGE('',*,*,#10806,.T.);
#15108=ORIENTED_EDGE('',*,*,#10804,.T.);
#15109=ORIENTED_EDGE('',*,*,#10806,.F.);
#15110=ORIENTED_EDGE('',*,*,#10807,.F.);
#15111=ORIENTED_EDGE('',*,*,#10808,.T.);
#15112=ORIENTED_EDGE('',*,*,#10805,.T.);
#15113=ORIENTED_EDGE('',*,*,#10808,.F.);
#15114=ORIENTED_EDGE('',*,*,#10809,.F.);
#15115=ORIENTED_EDGE('',*,*,#10810,.T.);
#15116=ORIENTED_EDGE('',*,*,#10807,.T.);
#15117=ORIENTED_EDGE('',*,*,#10810,.F.);
#15118=ORIENTED_EDGE('',*,*,#10809,.T.);
#15119=ORIENTED_EDGE('',*,*,#10811,.T.);
#15120=ORIENTED_EDGE('',*,*,#10812,.T.);
#15121=ORIENTED_EDGE('',*,*,#10813,.T.);
#15122=ORIENTED_EDGE('',*,*,#10814,.F.);
#15123=ORIENTED_EDGE('',*,*,#10815,.T.);
#15124=ORIENTED_EDGE('',*,*,#10816,.T.);
#15125=ORIENTED_EDGE('',*,*,#10817,.T.);
#15126=ORIENTED_EDGE('',*,*,#10812,.F.);
#15127=ORIENTED_EDGE('',*,*,#10818,.T.);
#15128=ORIENTED_EDGE('',*,*,#10819,.T.);
#15129=ORIENTED_EDGE('',*,*,#10820,.T.);
#15130=ORIENTED_EDGE('',*,*,#10816,.F.);
#15131=ORIENTED_EDGE('',*,*,#10821,.T.);
#15132=ORIENTED_EDGE('',*,*,#10822,.T.);
#15133=ORIENTED_EDGE('',*,*,#10823,.T.);
#15134=ORIENTED_EDGE('',*,*,#10819,.F.);
#15135=ORIENTED_EDGE('',*,*,#10824,.T.);
#15136=ORIENTED_EDGE('',*,*,#10825,.T.);
#15137=ORIENTED_EDGE('',*,*,#10826,.T.);
#15138=ORIENTED_EDGE('',*,*,#10822,.F.);
#15139=ORIENTED_EDGE('',*,*,#10827,.T.);
#15140=ORIENTED_EDGE('',*,*,#10814,.T.);
#15141=ORIENTED_EDGE('',*,*,#10828,.T.);
#15142=ORIENTED_EDGE('',*,*,#10825,.F.);
#15143=ORIENTED_EDGE('',*,*,#10827,.F.);
#15144=ORIENTED_EDGE('',*,*,#10824,.F.);
#15145=ORIENTED_EDGE('',*,*,#10821,.F.);
#15146=ORIENTED_EDGE('',*,*,#10818,.F.);
#15147=ORIENTED_EDGE('',*,*,#10815,.F.);
#15148=ORIENTED_EDGE('',*,*,#10811,.F.);
#15149=ORIENTED_EDGE('',*,*,#10828,.F.);
#15150=ORIENTED_EDGE('',*,*,#10813,.F.);
#15151=ORIENTED_EDGE('',*,*,#10817,.F.);
#15152=ORIENTED_EDGE('',*,*,#10820,.F.);
#15153=ORIENTED_EDGE('',*,*,#10823,.F.);
#15154=ORIENTED_EDGE('',*,*,#10826,.F.);
#15429=CYLINDRICAL_SURFACE('',#18688,0.35);
#15430=CYLINDRICAL_SURFACE('',#18696,0.1954);
#16348=ADVANCED_FACE('',(#3038),#2110,.T.);
#16349=ADVANCED_FACE('',(#3039),#1047,.T.);
#16350=ADVANCED_FACE('',(#3040),#15429,.T.);
#16351=ADVANCED_FACE('',(#3041),#1048,.T.);
#16352=ADVANCED_FACE('',(#3042,#1630),#2111,.T.);
#16353=ADVANCED_FACE('',(#3043),#1049,.T.);
#16354=ADVANCED_FACE('',(#3044),#15430,.T.);
#16355=ADVANCED_FACE('',(#3045),#1050,.T.);
#16356=ADVANCED_FACE('',(#3046),#2112,.T.);
#16357=ADVANCED_FACE('',(#3047),#2113,.F.);
#16358=ADVANCED_FACE('',(#3048),#2114,.F.);
#16359=ADVANCED_FACE('',(#3049),#2115,.F.);
#16360=ADVANCED_FACE('',(#3050),#2116,.F.);
#16361=ADVANCED_FACE('',(#3051),#2117,.F.);
#16362=ADVANCED_FACE('',(#3052),#2118,.F.);
#16363=ADVANCED_FACE('',(#3053),#2119,.F.);
#16364=ADVANCED_FACE('',(#3054),#2120,.F.);
#16450=CLOSED_SHELL('',(#16348,#16349,#16350,#16351,#16352,#16353,#16354,
#16355,#16356));
#16451=CLOSED_SHELL('',(#16357,#16358,#16359,#16360,#16361,#16362,#16363,
#16364));
#18683=AXIS2_PLACEMENT_3D('',#62413,#22987,#22988);
#18684=AXIS2_PLACEMENT_3D('',#62414,#22989,#22990);
#18685=AXIS2_PLACEMENT_3D('',#62416,#22991,#22992);
#18686=AXIS2_PLACEMENT_3D('',#62417,#22993,#22994);
#18687=AXIS2_PLACEMENT_3D('',#62419,#22995,#22996);
#18688=AXIS2_PLACEMENT_3D('',#62421,#22998,#22999);
#18689=AXIS2_PLACEMENT_3D('',#62423,#23000,#23001);
#18690=AXIS2_PLACEMENT_3D('',#62425,#23003,#23004);
#18691=AXIS2_PLACEMENT_3D('',#62427,#23005,#23006);
#18692=AXIS2_PLACEMENT_3D('',#62429,#23008,#23009);
#18693=AXIS2_PLACEMENT_3D('',#62431,#23010,#23011);
#18694=AXIS2_PLACEMENT_3D('',#62432,#23012,#23013);
#18695=AXIS2_PLACEMENT_3D('',#62434,#23014,#23015);
#18696=AXIS2_PLACEMENT_3D('',#62436,#23017,#23018);
#18697=AXIS2_PLACEMENT_3D('',#62438,#23019,#23020);
#18698=AXIS2_PLACEMENT_3D('',#62440,#23022,#23023);
#18699=AXIS2_PLACEMENT_3D('',#62442,#23024,#23025);
#18700=AXIS2_PLACEMENT_3D('',#62444,#23027,#23028);
#18701=AXIS2_PLACEMENT_3D('',#62445,#23029,#23030);
#18702=AXIS2_PLACEMENT_3D('',#62454,#23035,#23036);
#18703=AXIS2_PLACEMENT_3D('',#62460,#23040,#23041);
#18704=AXIS2_PLACEMENT_3D('',#62466,#23045,#23046);
#18705=AXIS2_PLACEMENT_3D('',#62472,#23050,#23051);
#18706=AXIS2_PLACEMENT_3D('',#62478,#23055,#23056);
#18707=AXIS2_PLACEMENT_3D('',#62481,#23059,#23060);
#18708=AXIS2_PLACEMENT_3D('',#62482,#23061,#23062);
#22987=DIRECTION('axis',(0.,0.,1.));
#22988=DIRECTION('refdir',(1.,0.,0.));
#22989=DIRECTION('center_axis',(0.,1.,0.));
#22990=DIRECTION('ref_axis',(0.,0.,1.));
#22991=DIRECTION('center_axis',(0.,-1.,0.));
#22992=DIRECTION('ref_axis',(1.,0.,0.));
#22993=DIRECTION('center_axis',(0.,-1.,0.));
#22994=DIRECTION('ref_axis',(1.,0.,0.));
#22995=DIRECTION('center_axis',(0.,-1.,0.));
#22996=DIRECTION('ref_axis',(1.,0.,0.));
#22997=DIRECTION('',(0.707106781186547,0.707106781186548,8.65956056235493E-17));
#22998=DIRECTION('center_axis',(0.,-1.,0.));
#22999=DIRECTION('ref_axis',(1.,0.,0.));
#23000=DIRECTION('center_axis',(0.,-1.,0.));
#23001=DIRECTION('ref_axis',(1.,0.,0.));
#23002=DIRECTION('',(0.,1.,0.));
#23003=DIRECTION('center_axis',(0.,1.,0.));
#23004=DIRECTION('ref_axis',(1.,0.,0.));
#23005=DIRECTION('center_axis',(0.,-1.,0.));
#23006=DIRECTION('ref_axis',(1.,0.,0.));
#23007=DIRECTION('',(-0.707106781186547,0.707106781186548,-8.65956056235493E-17));
#23008=DIRECTION('center_axis',(0.,-1.,0.));
#23009=DIRECTION('ref_axis',(0.,0.,-1.));
#23010=DIRECTION('center_axis',(0.,-1.,0.));
#23011=DIRECTION('ref_axis',(1.,0.,0.));
#23012=DIRECTION('center_axis',(0.,1.,0.));
#23013=DIRECTION('ref_axis',(1.,0.,0.));
#23014=DIRECTION('center_axis',(0.,1.,0.));
#23015=DIRECTION('ref_axis',(1.,0.,0.));
#23016=DIRECTION('',(-0.447213595499958,0.894427190999916,-5.47678698264203E-17));
#23017=DIRECTION('center_axis',(0.,-1.,0.));
#23018=DIRECTION('ref_axis',(1.,0.,0.));
#23019=DIRECTION('center_axis',(0.,1.,0.));
#23020=DIRECTION('ref_axis',(1.,0.,0.));
#23021=DIRECTION('',(0.,1.,0.));
#23022=DIRECTION('center_axis',(0.,1.,0.));
#23023=DIRECTION('ref_axis',(1.,0.,0.));
#23024=DIRECTION('center_axis',(0.,-1.,0.));
#23025=DIRECTION('ref_axis',(1.,0.,0.));
#23026=DIRECTION('',(-0.707106781186547,0.707106781186548,-8.65956056235493E-17));
#23027=DIRECTION('center_axis',(0.,-1.,0.));
#23028=DIRECTION('ref_axis',(0.,0.,-1.));
#23029=DIRECTION('center_axis',(0.866025403784439,0.,-0.5));
#23030=DIRECTION('ref_axis',(0.5,0.,0.866025403784439));
#23031=DIRECTION('',(-0.5,0.,-0.866025403784439));
#23032=DIRECTION('',(0.,-1.,0.));
#23033=DIRECTION('',(0.5,0.,0.866025403784439));
#23034=DIRECTION('',(0.,-1.,0.));
#23035=DIRECTION('center_axis',(1.60246890531964E-16,0.,-1.));
#23036=DIRECTION('ref_axis',(1.,0.,1.60246890531964E-16));
#23037=DIRECTION('',(-1.,0.,-1.60246890531964E-16));
#23038=DIRECTION('',(0.,-1.,0.));
#23039=DIRECTION('',(1.,0.,1.60246890531964E-16));
#23040=DIRECTION('center_axis',(-0.866025403784439,0.,-0.5));
#23041=DIRECTION('ref_axis',(0.5,0.,-0.866025403784439));
#23042=DIRECTION('',(-0.5,0.,0.866025403784439));
#23043=DIRECTION('',(0.,-1.,0.));
#23044=DIRECTION('',(0.5,0.,-0.866025403784439));
#23045=DIRECTION('center_axis',(-0.866025403784439,0.,0.5));
#23046=DIRECTION('ref_axis',(-0.5,0.,-0.866025403784439));
#23047=DIRECTION('',(0.5,0.,0.866025403784439));
#23048=DIRECTION('',(0.,-1.,0.));
#23049=DIRECTION('',(-0.5,0.,-0.866025403784439));
#23050=DIRECTION('center_axis',(-1.60246890531964E-16,0.,1.));
#23051=DIRECTION('ref_axis',(-1.,0.,-1.60246890531964E-16));
#23052=DIRECTION('',(1.,0.,1.60246890531964E-16));
#23053=DIRECTION('',(0.,-1.,0.));
#23054=DIRECTION('',(-1.,0.,-1.60246890531964E-16));
#23055=DIRECTION('center_axis',(0.866025403784439,0.,0.5));
#23056=DIRECTION('ref_axis',(-0.5,0.,0.866025403784439));
#23057=DIRECTION('',(0.5,0.,-0.866025403784439));
#23058=DIRECTION('',(-0.5,0.,0.866025403784439));
#23059=DIRECTION('center_axis',(0.,1.,0.));
#23060=DIRECTION('ref_axis',(1.,0.,0.));
#23061=DIRECTION('center_axis',(0.,-1.,0.));
#23062=DIRECTION('ref_axis',(0.,0.,-1.));
#62413=CARTESIAN_POINT('',(0.,0.,0.));
#62414=CARTESIAN_POINT('Origin',(0.3,0.4,0.));
#62415=CARTESIAN_POINT('',(-0.3,0.4,-3.67394039744206E-17));
#62416=CARTESIAN_POINT('Origin',(0.,0.4,0.));
#62417=CARTESIAN_POINT('Origin',(0.,0.375,0.));
#62418=CARTESIAN_POINT('',(-0.35,0.35,-4.28626379701573E-17));
#62419=CARTESIAN_POINT('Origin',(0.,0.35,0.));
#62420=CARTESIAN_POINT('',(-0.325,0.375,-3.9801020972289E-17));
#62421=CARTESIAN_POINT('Origin',(0.,0.19,0.));
#62422=CARTESIAN_POINT('',(-0.35,0.03,-4.28626379701574E-17));
#62423=CARTESIAN_POINT('Origin',(0.,0.03,0.));
#62424=CARTESIAN_POINT('',(-0.35,0.19,-4.28626379701574E-17));
#62425=CARTESIAN_POINT('Origin',(0.,0.0149999999999999,0.));
#62426=CARTESIAN_POINT('',(-0.32,-3.29597460435593E-17,-3.91886975727153E-17));
#62427=CARTESIAN_POINT('Origin',(0.,0.,0.));
#62428=CARTESIAN_POINT('',(-0.335,0.0149999999999999,-4.10256677714363E-17));
#62429=CARTESIAN_POINT('Origin',(0.22,0.,0.));
#62430=CARTESIAN_POINT('',(-0.22,-6.93889390390723E-18,-2.69422295812418E-17));
#62431=CARTESIAN_POINT('Origin',(0.,0.,0.));
#62432=CARTESIAN_POINT('Origin',(0.,-0.02,0.));
#62433=CARTESIAN_POINT('',(-0.1954,-0.0492,2.39295984553393E-17));
#62434=CARTESIAN_POINT('Origin',(0.,-0.0492,0.));
#62435=CARTESIAN_POINT('',(-0.21,-0.02,-2.57175827820944E-17));
#62436=CARTESIAN_POINT('Origin',(0.,-0.8,0.));
#62437=CARTESIAN_POINT('',(-0.1954,-1.5646,2.39295984553393E-17));
#62438=CARTESIAN_POINT('Origin',(0.,-1.5646,0.));
#62439=CARTESIAN_POINT('',(-0.1954,-0.8,-2.39295984553393E-17));
#62440=CARTESIAN_POINT('Origin',(0.,-1.58,0.));
#62441=CARTESIAN_POINT('',(-0.16,-1.6,-1.95943487863577E-17));
#62442=CARTESIAN_POINT('Origin',(0.,-1.6,0.));
#62443=CARTESIAN_POINT('',(-0.18,-1.58,-2.20436423846524E-17));
#62444=CARTESIAN_POINT('Origin',(0.,-1.6,0.));
#62445=CARTESIAN_POINT('Origin',(0.0866025403784439,-0.4,-0.15));
#62446=CARTESIAN_POINT('',(0.173205080756888,-0.4,0.));
#62447=CARTESIAN_POINT('',(0.0866025403784439,-0.4,-0.15));
#62448=CARTESIAN_POINT('',(0.173205080756888,-0.4,0.));
#62449=CARTESIAN_POINT('',(0.0866025403784439,-0.64,-0.15));
#62450=CARTESIAN_POINT('',(0.0866025403784439,-0.4,-0.15));
#62451=CARTESIAN_POINT('',(0.173205080756888,-0.64,0.));
#62452=CARTESIAN_POINT('',(0.173205080756888,-0.64,0.));
#62453=CARTESIAN_POINT('',(0.173205080756888,-0.4,0.));
#62454=CARTESIAN_POINT('Origin',(-0.0866025403784438,-0.4,-0.15));
#62455=CARTESIAN_POINT('',(-0.0866025403784438,-0.4,-0.15));
#62456=CARTESIAN_POINT('',(0.0866025403784439,-0.4,-0.15));
#62457=CARTESIAN_POINT('',(-0.0866025403784438,-0.64,-0.15));
#62458=CARTESIAN_POINT('',(-0.0866025403784438,-0.4,-0.15));
#62459=CARTESIAN_POINT('',(0.0866025403784439,-0.64,-0.15));
#62460=CARTESIAN_POINT('Origin',(-0.173205080756888,-0.4,-2.77555756156289E-17));
#62461=CARTESIAN_POINT('',(-0.173205080756888,-0.4,-2.12115047744981E-17));
#62462=CARTESIAN_POINT('',(-0.0866025403784438,-0.4,-0.15));
#62463=CARTESIAN_POINT('',(-0.173205080756888,-0.64,-2.77555756156289E-17));
#62464=CARTESIAN_POINT('',(-0.173205080756888,-0.4,-2.12115047744981E-17));
#62465=CARTESIAN_POINT('',(-0.0866025403784438,-0.64,-0.15));
#62466=CARTESIAN_POINT('Origin',(-0.0866025403784439,-0.4,0.15));
#62467=CARTESIAN_POINT('',(-0.0866025403784439,-0.4,0.15));
#62468=CARTESIAN_POINT('',(-0.173205080756888,-0.4,-2.12115047744981E-17));
#62469=CARTESIAN_POINT('',(-0.0866025403784439,-0.64,0.15));
#62470=CARTESIAN_POINT('',(-0.0866025403784439,-0.4,0.15));
#62471=CARTESIAN_POINT('',(-0.173205080756888,-0.64,-2.12115047744981E-17));
#62472=CARTESIAN_POINT('Origin',(0.0866025403784439,-0.4,0.15));
#62473=CARTESIAN_POINT('',(0.0866025403784439,-0.4,0.15));
#62474=CARTESIAN_POINT('',(-0.0866025403784439,-0.4,0.15));
#62475=CARTESIAN_POINT('',(0.0866025403784439,-0.64,0.15));
#62476=CARTESIAN_POINT('',(0.0866025403784439,-0.4,0.15));
#62477=CARTESIAN_POINT('',(-0.0866025403784439,-0.64,0.15));
#62478=CARTESIAN_POINT('Origin',(0.173205080756888,-0.4,0.));
#62479=CARTESIAN_POINT('',(0.0866025403784439,-0.4,0.15));
#62480=CARTESIAN_POINT('',(0.0866025403784439,-0.64,0.15));
#62481=CARTESIAN_POINT('Origin',(0.,-0.4,-2.77555756156289E-17));
#62482=CARTESIAN_POINT('Origin',(0.,-0.64,-2.77555756156289E-17));
#62681=UNCERTAINTY_MEASURE_WITH_UNIT(LENGTH_MEASURE(0.001),#62759,
'DISTANCE_ACCURACY_VALUE',
'Maximum model space distance between geometric entities at asserted c
onnectivities');
#62684=UNCERTAINTY_MEASURE_WITH_UNIT(LENGTH_MEASURE(0.001),#62759,
'DISTANCE_ACCURACY_VALUE',
'Maximum model space distance between geometric entities at asserted c
onnectivities');
#62755=(
GEOMETRIC_REPRESENTATION_CONTEXT(3)
GLOBAL_UNCERTAINTY_ASSIGNED_CONTEXT((#62681))
GLOBAL_UNIT_ASSIGNED_CONTEXT((#62759,#62761,#62762))
REPRESENTATION_CONTEXT('','3D')
);
#62758=(
GEOMETRIC_REPRESENTATION_CONTEXT(3)
GLOBAL_UNCERTAINTY_ASSIGNED_CONTEXT((#62684))
GLOBAL_UNIT_ASSIGNED_CONTEXT((#62759,#62761,#62762))
REPRESENTATION_CONTEXT('','3D')
);
#62759=(
LENGTH_UNIT()
NAMED_UNIT(*)
SI_UNIT(.CENTI.,.METRE.)
);
#62761=(
NAMED_UNIT(*)
PLANE_ANGLE_UNIT()
SI_UNIT($,.RADIAN.)
);
#62762=(
NAMED_UNIT(*)
SI_UNIT($,.STERADIAN.)
SOLID_ANGLE_UNIT()
);
#62833=SHAPE_DEFINITION_REPRESENTATION(#62916,#63101);
#62916=PRODUCT_DEFINITION_SHAPE('',$,#63175);
#63101=SHAPE_REPRESENTATION('',(#18683),#62755);
#63104=PRODUCT_DEFINITION_CONTEXT('part definition',#63325,'design');
#63175=PRODUCT_DEFINITION('Cap Screw - M4x16','Cap Screw - M4x16',#63248,
#63104);
#63248=PRODUCT_DEFINITION_FORMATION('',$,#63397);
#63325=APPLICATION_CONTEXT(
'Core Data for Automotive Mechanical Design Process');
#63326=PRODUCT_CONTEXT('part definition',#63325,'mechanical');
#63397=PRODUCT('Cap Screw - M4x16','Cap Screw - M4x16',
'Cap Screw - M4x16',(#63326));
#63463=COLOUR_RGB('Black',0.12,0.14,0.17);
#63464=FILL_AREA_STYLE_COLOUR('',#63463);
#63465=FILL_AREA_STYLE('',(#63464));
#63466=SURFACE_STYLE_FILL_AREA(#63465);
#63467=SURFACE_SIDE_STYLE('',(#63466));
#63468=SURFACE_STYLE_USAGE(.BOTH.,#63467);
#63469=PRESENTATION_STYLE_ASSIGNMENT((#63468));
ENDSEC;
END-ISO-10303-21;
